ISO-10303-21;
HEADER;
/* Generated by software containing ST-Developer
 * from STEP Tools, Inc. (www.steptools.com) 
 */

FILE_DESCRIPTION(
/* description */ ('Double-row support with tensioned shaft'),
/* implementation_level */ '2;1');

FILE_NAME(
/* name */ 'M6x18 mounting screw.step',
/* time_stamp */ '2026-10-27T10:50:35-07:00',
/* author */ (''),
/* organization */ (''),
/* preprocessor_version */ 'ST-DEVELOPER v20.2',
/* originating_system */ 'Autodesk Translation Framework v15.17.0.0',
/* authorisation */ '');

FILE_SCHEMA (('AUTOMOTIVE_DESIGN { 1 0 10303 214 3 1 1 }'));
ENDSEC;

DATA;
#10=MECHANICAL_DESIGN_GEOMETRIC_PRESENTATION_REPRESENTATION('',(#497),#11559);
#396=CONICAL_SURFACE('',#7026,0.475,0.785398163397449);
#397=CONICAL_SURFACE('',#7030,0.485,0.785398163397448);
#398=CONICAL_SURFACE('',#7034,0.31,0.463647609000806);
#408=ORIENTED_CLOSED_SHELL('',*,#6343,.F.);
#411=BREP_WITH_VOIDS('Body1',#6344,(#408));
#433=SHAPE_REPRESENTATION_RELATIONSHIP('SRR','None',#11741,#465);
#465=ADVANCED_BREP_SHAPE_REPRESENTATION('',(#411),#11543);
#497=STYLED_ITEM('',(#11974),#411);
#614=FACE_BOUND('',#1528,.T.);
#811=PLANE('',#7014);
#812=PLANE('',#7015);
#813=PLANE('',#7016);
#814=PLANE('',#7017);
#815=PLANE('',#7018);
#816=PLANE('',#7019);
#817=PLANE('',#7020);
#818=PLANE('',#7021);
#819=PLANE('',#7022);
#820=PLANE('',#7024);
#821=PLANE('',#7032);
#1098=FACE_OUTER_BOUND('',#1514,.T.);
#1099=FACE_OUTER_BOUND('',#1515,.T.);
#1100=FACE_OUTER_BOUND('',#1516,.T.);
#1101=FACE_OUTER_BOUND('',#1517,.T.);
#1102=FACE_OUTER_BOUND('',#1518,.T.);
#1103=FACE_OUTER_BOUND('',#1519,.T.);
#1104=FACE_OUTER_BOUND('',#1520,.T.);
#1105=FACE_OUTER_BOUND('',#1521,.T.);
#1106=FACE_OUTER_BOUND('',#1522,.T.);
#1107=FACE_OUTER_BOUND('',#1523,.T.);
#1108=FACE_OUTER_BOUND('',#1524,.T.);
#1109=FACE_OUTER_BOUND('',#1525,.T.);
#1110=FACE_OUTER_BOUND('',#1526,.T.);
#1111=FACE_OUTER_BOUND('',#1527,.T.);
#1112=FACE_OUTER_BOUND('',#1529,.T.);
#1113=FACE_OUTER_BOUND('',#1530,.T.);
#1514=EDGE_LOOP('',(#5182,#5183,#5184,#5185));
#1515=EDGE_LOOP('',(#5186,#5187,#5188,#5189));
#1516=EDGE_LOOP('',(#5190,#5191,#5192,#5193));
#1517=EDGE_LOOP('',(#5194,#5195,#5196,#5197));
#1518=EDGE_LOOP('',(#5198,#5199,#5200,#5201));
#1519=EDGE_LOOP('',(#5202,#5203,#5204,#5205));
#1520=EDGE_LOOP('',(#5206,#5207,#5208,#5209,#5210,#5211));
#1521=EDGE_LOOP('',(#5212,#5213,#5214,#5215,#5216,#5217));
#1522=EDGE_LOOP('',(#5218));
#1523=EDGE_LOOP('',(#5219));
#1524=EDGE_LOOP('',(#5220,#5221,#5222,#5223));
#1525=EDGE_LOOP('',(#5224,#5225,#5226,#5227));
#1526=EDGE_LOOP('',(#5228,#5229,#5230,#5231));
#1527=EDGE_LOOP('',(#5232));
#1528=EDGE_LOOP('',(#5233));
#1529=EDGE_LOOP('',(#5234,#5235,#5236,#5237));
#1530=EDGE_LOOP('',(#5238,#5239,#5240,#5241));
#2069=LINE('',#10148,#2616);
#2070=LINE('',#10150,#2617);
#2071=LINE('',#10152,#2618);
#2072=LINE('',#10153,#2619);
#2073=LINE('',#10156,#2620);
#2074=LINE('',#10158,#2621);
#2075=LINE('',#10159,#2622);
#2076=LINE('',#10162,#2623);
#2077=LINE('',#10164,#2624);
#2078=LINE('',#10165,#2625);
#2079=LINE('',#10168,#2626);
#2080=LINE('',#10170,#2627);
#2081=LINE('',#10171,#2628);
#2082=LINE('',#10174,#2629);
#2083=LINE('',#10176,#2630);
#2084=LINE('',#10177,#2631);
#2085=LINE('',#10179,#2632);
#2086=LINE('',#10180,#2633);
#2087=LINE('',#10192,#2634);
#2088=LINE('',#10196,#2635);
#2089=LINE('',#10200,#2636);
#2090=LINE('',#10207,#2637);
#2091=LINE('',#10209,#2638);
#2616=VECTOR('',#8302,1.);
#2617=VECTOR('',#8303,1.);
#2618=VECTOR('',#8304,1.);
#2619=VECTOR('',#8305,1.);
#2620=VECTOR('',#8308,1.);
#2621=VECTOR('',#8309,1.);
#2622=VECTOR('',#8310,1.);
#2623=VECTOR('',#8313,1.);
#2624=VECTOR('',#8314,1.);
#2625=VECTOR('',#8315,1.);
#2626=VECTOR('',#8318,1.);
#2627=VECTOR('',#8319,1.);
#2628=VECTOR('',#8320,1.);
#2629=VECTOR('',#8323,1.);
#2630=VECTOR('',#8324,1.);
#2631=VECTOR('',#8325,1.);
#2632=VECTOR('',#8328,1.);
#2633=VECTOR('',#8329,1.);
#2634=VECTOR('',#8346,0.475);
#2635=VECTOR('',#8351,0.5);
#2636=VECTOR('',#8356,0.485);
#2637=VECTOR('',#8365,0.31);
#2638=VECTOR('',#8368,0.3);
#2933=CIRCLE('',#7023,0.2942);
#2934=CIRCLE('',#7025,0.45);
#2935=CIRCLE('',#7027,0.5);
#2936=CIRCLE('',#7029,0.5);
#2937=CIRCLE('',#7031,0.47);
#2938=CIRCLE('',#7033,0.32);
#2939=CIRCLE('',#7035,0.2942);
#3310=VERTEX_POINT('',#10146);
#3311=VERTEX_POINT('',#10147);
#3312=VERTEX_POINT('',#10149);
#3313=VERTEX_POINT('',#10151);
#3314=VERTEX_POINT('',#10155);
#3315=VERTEX_POINT('',#10157);
#3316=VERTEX_POINT('',#10161);
#3317=VERTEX_POINT('',#10163);
#3318=VERTEX_POINT('',#10167);
#3319=VERTEX_POINT('',#10169);
#3320=VERTEX_POINT('',#10173);
#3321=VERTEX_POINT('',#10175);
#3322=VERTEX_POINT('',#10184);
#3323=VERTEX_POINT('',#10187);
#3324=VERTEX_POINT('',#10190);
#3325=VERTEX_POINT('',#10194);
#3326=VERTEX_POINT('',#10198);
#3327=VERTEX_POINT('',#10202);
#3328=VERTEX_POINT('',#10205);
#3976=EDGE_CURVE('',#3310,#3311,#2069,.T.);
#3977=EDGE_CURVE('',#3311,#3312,#2070,.T.);
#3978=EDGE_CURVE('',#3312,#3313,#2071,.T.);
#3979=EDGE_CURVE('',#3310,#3313,#2072,.T.);
#3980=EDGE_CURVE('',#3311,#3314,#2073,.T.);
#3981=EDGE_CURVE('',#3314,#3315,#2074,.T.);
#3982=EDGE_CURVE('',#3315,#3312,#2075,.T.);
#3983=EDGE_CURVE('',#3314,#3316,#2076,.T.);
#3984=EDGE_CURVE('',#3316,#3317,#2077,.T.);
#3985=EDGE_CURVE('',#3317,#3315,#2078,.T.);
#3986=EDGE_CURVE('',#3316,#3318,#2079,.T.);
#3987=EDGE_CURVE('',#3318,#3319,#2080,.T.);
#3988=EDGE_CURVE('',#3319,#3317,#2081,.T.);
#3989=EDGE_CURVE('',#3318,#3320,#2082,.T.);
#3990=EDGE_CURVE('',#3320,#3321,#2083,.T.);
#3991=EDGE_CURVE('',#3321,#3319,#2084,.T.);
#3992=EDGE_CURVE('',#3320,#3310,#2085,.T.);
#3993=EDGE_CURVE('',#3313,#3321,#2086,.T.);
#3994=EDGE_CURVE('',#3322,#3322,#2933,.T.);
#3995=EDGE_CURVE('',#3323,#3323,#2934,.T.);
#3996=EDGE_CURVE('',#3324,#3324,#2935,.T.);
#3997=EDGE_CURVE('',#3324,#3323,#2087,.T.);
#3998=EDGE_CURVE('',#3325,#3325,#2936,.T.);
#3999=EDGE_CURVE('',#3325,#3324,#2088,.T.);
#4000=EDGE_CURVE('',#3326,#3326,#2937,.T.);
#4001=EDGE_CURVE('',#3326,#3325,#2089,.T.);
#4002=EDGE_CURVE('',#3327,#3327,#2938,.T.);
#4003=EDGE_CURVE('',#3328,#3328,#2939,.F.);
#4004=EDGE_CURVE('',#3328,#3327,#2090,.T.);
#4005=EDGE_CURVE('',#3322,#3328,#2091,.T.);
#5182=ORIENTED_EDGE('',*,*,#3976,.T.);
#5183=ORIENTED_EDGE('',*,*,#3977,.T.);
#5184=ORIENTED_EDGE('',*,*,#3978,.T.);
#5185=ORIENTED_EDGE('',*,*,#3979,.F.);
#5186=ORIENTED_EDGE('',*,*,#3980,.T.);
#5187=ORIENTED_EDGE('',*,*,#3981,.T.);
#5188=ORIENTED_EDGE('',*,*,#3982,.T.);
#5189=ORIENTED_EDGE('',*,*,#3977,.F.);
#5190=ORIENTED_EDGE('',*,*,#3983,.T.);
#5191=ORIENTED_EDGE('',*,*,#3984,.T.);
#5192=ORIENTED_EDGE('',*,*,#3985,.T.);
#5193=ORIENTED_EDGE('',*,*,#3981,.F.);
#5194=ORIENTED_EDGE('',*,*,#3986,.T.);
#5195=ORIENTED_EDGE('',*,*,#3987,.T.);
#5196=ORIENTED_EDGE('',*,*,#3988,.T.);
#5197=ORIENTED_EDGE('',*,*,#3984,.F.);
#5198=ORIENTED_EDGE('',*,*,#3989,.T.);
#5199=ORIENTED_EDGE('',*,*,#3990,.T.);
#5200=ORIENTED_EDGE('',*,*,#3991,.T.);
#5201=ORIENTED_EDGE('',*,*,#3987,.F.);
#5202=ORIENTED_EDGE('',*,*,#3992,.T.);
#5203=ORIENTED_EDGE('',*,*,#3979,.T.);
#5204=ORIENTED_EDGE('',*,*,#3993,.T.);
#5205=ORIENTED_EDGE('',*,*,#3990,.F.);
#5206=ORIENTED_EDGE('',*,*,#3992,.F.);
#5207=ORIENTED_EDGE('',*,*,#3989,.F.);
#5208=ORIENTED_EDGE('',*,*,#3986,.F.);
#5209=ORIENTED_EDGE('',*,*,#3983,.F.);
#5210=ORIENTED_EDGE('',*,*,#3980,.F.);
#5211=ORIENTED_EDGE('',*,*,#3976,.F.);
#5212=ORIENTED_EDGE('',*,*,#3993,.F.);
#5213=ORIENTED_EDGE('',*,*,#3978,.F.);
#5214=ORIENTED_EDGE('',*,*,#3982,.F.);
#5215=ORIENTED_EDGE('',*,*,#3985,.F.);
#5216=ORIENTED_EDGE('',*,*,#3988,.F.);
#5217=ORIENTED_EDGE('',*,*,#3991,.F.);
#5218=ORIENTED_EDGE('',*,*,#3994,.F.);
#5219=ORIENTED_EDGE('',*,*,#3995,.F.);
#5220=ORIENTED_EDGE('',*,*,#3996,.F.);
#5221=ORIENTED_EDGE('',*,*,#3997,.T.);
#5222=ORIENTED_EDGE('',*,*,#3995,.T.);
#5223=ORIENTED_EDGE('',*,*,#3997,.F.);
#5224=ORIENTED_EDGE('',*,*,#3998,.F.);
#5225=ORIENTED_EDGE('',*,*,#3999,.T.);
#5226=ORIENTED_EDGE('',*,*,#3996,.T.);
#5227=ORIENTED_EDGE('',*,*,#3999,.F.);
#5228=ORIENTED_EDGE('',*,*,#4000,.F.);
#5229=ORIENTED_EDGE('',*,*,#4001,.T.);
#5230=ORIENTED_EDGE('',*,*,#3998,.T.);
#5231=ORIENTED_EDGE('',*,*,#4001,.F.);
#5232=ORIENTED_EDGE('',*,*,#4000,.T.);
#5233=ORIENTED_EDGE('',*,*,#4002,.F.);
#5234=ORIENTED_EDGE('',*,*,#4003,.F.);
#5235=ORIENTED_EDGE('',*,*,#4004,.T.);
#5236=ORIENTED_EDGE('',*,*,#4002,.T.);
#5237=ORIENTED_EDGE('',*,*,#4004,.F.);
#5238=ORIENTED_EDGE('',*,*,#3994,.T.);
#5239=ORIENTED_EDGE('',*,*,#4005,.T.);
#5240=ORIENTED_EDGE('',*,*,#4003,.T.);
#5241=ORIENTED_EDGE('',*,*,#4005,.F.);
#5936=CYLINDRICAL_SURFACE('',#7028,0.5);
#5937=CYLINDRICAL_SURFACE('',#7036,0.2942);
#6161=ADVANCED_FACE('',(#1098),#811,.F.);
#6162=ADVANCED_FACE('',(#1099),#812,.F.);
#6163=ADVANCED_FACE('',(#1100),#813,.F.);
#6164=ADVANCED_FACE('',(#1101),#814,.F.);
#6165=ADVANCED_FACE('',(#1102),#815,.F.);
#6166=ADVANCED_FACE('',(#1103),#816,.F.);
#6167=ADVANCED_FACE('',(#1104),#817,.F.);
#6168=ADVANCED_FACE('',(#1105),#818,.F.);
#6169=ADVANCED_FACE('',(#1106),#819,.F.);
#6170=ADVANCED_FACE('',(#1107),#820,.T.);
#6171=ADVANCED_FACE('',(#1108),#396,.T.);
#6172=ADVANCED_FACE('',(#1109),#5936,.T.);
#6173=ADVANCED_FACE('',(#1110),#397,.T.);
#6174=ADVANCED_FACE('',(#1111,#614),#821,.T.);
#6175=ADVANCED_FACE('',(#1112),#398,.T.);
#6176=ADVANCED_FACE('',(#1113),#5937,.T.);
#6343=CLOSED_SHELL('',(#6161,#6162,#6163,#6164,#6165,#6166,#6167,#6168));
#6344=CLOSED_SHELL('',(#6169,#6170,#6171,#6172,#6173,#6174,#6175,#6176));
#7013=AXIS2_PLACEMENT_3D('',#10144,#8298,#8299);
#7014=AXIS2_PLACEMENT_3D('',#10145,#8300,#8301);
#7015=AXIS2_PLACEMENT_3D('',#10154,#8306,#8307);
#7016=AXIS2_PLACEMENT_3D('',#10160,#8311,#8312);
#7017=AXIS2_PLACEMENT_3D('',#10166,#8316,#8317);
#7018=AXIS2_PLACEMENT_3D('',#10172,#8321,#8322);
#7019=AXIS2_PLACEMENT_3D('',#10178,#8326,#8327);
#7020=AXIS2_PLACEMENT_3D('',#10181,#8330,#8331);
#7021=AXIS2_PLACEMENT_3D('',#10182,#8332,#8333);
#7022=AXIS2_PLACEMENT_3D('',#10183,#8334,#8335);
#7023=AXIS2_PLACEMENT_3D('',#10185,#8336,#8337);
#7024=AXIS2_PLACEMENT_3D('',#10186,#8338,#8339);
#7025=AXIS2_PLACEMENT_3D('',#10188,#8340,#8341);
#7026=AXIS2_PLACEMENT_3D('',#10189,#8342,#8343);
#7027=AXIS2_PLACEMENT_3D('',#10191,#8344,#8345);
#7028=AXIS2_PLACEMENT_3D('',#10193,#8347,#8348);
#7029=AXIS2_PLACEMENT_3D('',#10195,#8349,#8350);
#7030=AXIS2_PLACEMENT_3D('',#10197,#8352,#8353);
#7031=AXIS2_PLACEMENT_3D('',#10199,#8354,#8355);
#7032=AXIS2_PLACEMENT_3D('',#10201,#8357,#8358);
#7033=AXIS2_PLACEMENT_3D('',#10203,#8359,#8360);
#7034=AXIS2_PLACEMENT_3D('',#10204,#8361,#8362);
#7035=AXIS2_PLACEMENT_3D('',#10206,#8363,#8364);
#7036=AXIS2_PLACEMENT_3D('',#10208,#8366,#8367);
#8298=DIRECTION('axis',(0.,0.,1.));
#8299=DIRECTION('refdir',(1.,0.,0.));
#8300=DIRECTION('center_axis',(0.866025403784439,0.,-0.5));
#8301=DIRECTION('ref_axis',(0.5,0.,0.866025403784439));
#8302=DIRECTION('',(-0.5,0.,-0.866025403784439));
#8303=DIRECTION('',(0.,-1.,0.));
#8304=DIRECTION('',(0.5,0.,0.866025403784439));
#8305=DIRECTION('',(0.,-1.,0.));
#8306=DIRECTION('center_axis',(1.92296268638356E-16,0.,-1.));
#8307=DIRECTION('ref_axis',(1.,0.,1.92296268638356E-16));
#8308=DIRECTION('',(-1.,0.,-1.92296268638356E-16));
#8309=DIRECTION('',(0.,-1.,0.));
#8310=DIRECTION('',(1.,0.,1.92296268638356E-16));
#8311=DIRECTION('center_axis',(-0.866025403784439,0.,-0.5));
#8312=DIRECTION('ref_axis',(0.5,0.,-0.866025403784439));
#8313=DIRECTION('',(-0.5,0.,0.866025403784438));
#8314=DIRECTION('',(0.,-1.,0.));
#8315=DIRECTION('',(0.5,0.,-0.866025403784438));
#8316=DIRECTION('center_axis',(-0.866025403784439,0.,0.5));
#8317=DIRECTION('ref_axis',(-0.5,0.,-0.866025403784439));
#8318=DIRECTION('',(0.5,0.,0.866025403784439));
#8319=DIRECTION('',(0.,-1.,0.));
#8320=DIRECTION('',(-0.5,0.,-0.866025403784439));
#8321=DIRECTION('center_axis',(-1.92296268638356E-16,0.,1.));
#8322=DIRECTION('ref_axis',(-1.,0.,-1.92296268638356E-16));
#8323=DIRECTION('',(1.,0.,1.92296268638356E-16));
#8324=DIRECTION('',(0.,-1.,0.));
#8325=DIRECTION('',(-1.,0.,-1.92296268638356E-16));
#8326=DIRECTION('center_axis',(0.866025403784439,0.,0.5));
#8327=DIRECTION('ref_axis',(-0.5,0.,0.866025403784439));
#8328=DIRECTION('',(0.5,0.,-0.866025403784439));
#8329=DIRECTION('',(-0.5,0.,0.866025403784439));
#8330=DIRECTION('center_axis',(0.,1.,0.));
#8331=DIRECTION('ref_axis',(1.,0.,0.));
#8332=DIRECTION('center_axis',(0.,-1.,0.));
#8333=DIRECTION('ref_axis',(0.,0.,-1.));
#8334=DIRECTION('center_axis',(0.,1.,0.));
#8335=DIRECTION('ref_axis',(1.,0.,0.));
#8336=DIRECTION('center_axis',(0.,1.,0.));
#8337=DIRECTION('ref_axis',(1.,0.,0.));
#8338=DIRECTION('center_axis',(0.,1.,0.));
#8339=DIRECTION('ref_axis',(0.,0.,1.));
#8340=DIRECTION('center_axis',(0.,-1.,0.));
#8341=DIRECTION('ref_axis',(1.,0.,0.));
#8342=DIRECTION('center_axis',(0.,-1.,0.));
#8343=DIRECTION('ref_axis',(1.,0.,0.));
#8344=DIRECTION('center_axis',(0.,-1.,0.));
#8345=DIRECTION('ref_axis',(1.,0.,0.));
#8346=DIRECTION('',(0.707106781186548,0.707106781186547,8.65956056235494E-17));
#8347=DIRECTION('center_axis',(0.,-1.,0.));
#8348=DIRECTION('ref_axis',(1.,0.,0.));
#8349=DIRECTION('center_axis',(0.,-1.,0.));
#8350=DIRECTION('ref_axis',(1.,0.,0.));
#8351=DIRECTION('',(0.,1.,0.));
#8352=DIRECTION('center_axis',(0.,1.,0.));
#8353=DIRECTION('ref_axis',(1.,0.,0.));
#8354=DIRECTION('center_axis',(0.,-1.,0.));
#8355=DIRECTION('ref_axis',(1.,0.,0.));
#8356=DIRECTION('',(-0.707106781186547,0.707106781186548,-8.65956056235493E-17));
#8357=DIRECTION('center_axis',(0.,-1.,0.));
#8358=DIRECTION('ref_axis',(0.,0.,-1.));
#8359=DIRECTION('center_axis',(0.,-1.,0.));
#8360=DIRECTION('ref_axis',(1.,0.,0.));
#8361=DIRECTION('center_axis',(0.,1.,0.));
#8362=DIRECTION('ref_axis',(1.,0.,0.));
#8363=DIRECTION('center_axis',(0.,1.,0.));
#8364=DIRECTION('ref_axis',(1.,0.,0.));
#8365=DIRECTION('',(-0.447213595499958,0.894427190999916,-5.47678698264203E-17));
#8366=DIRECTION('center_axis',(0.,-1.,0.));
#8367=DIRECTION('ref_axis',(1.,0.,0.));
#8368=DIRECTION('',(0.,1.,0.));
#10144=CARTESIAN_POINT('',(0.,0.,0.));
#10145=CARTESIAN_POINT('Origin',(0.144337567297406,-0.6,-0.25));
#10146=CARTESIAN_POINT('',(0.288675134594813,-0.6,0.));
#10147=CARTESIAN_POINT('',(0.144337567297406,-0.6,-0.25));
#10148=CARTESIAN_POINT('',(0.288675134594813,-0.6,0.));
#10149=CARTESIAN_POINT('',(0.144337567297406,-0.96,-0.25));
#10150=CARTESIAN_POINT('',(0.144337567297406,-0.6,-0.25));
#10151=CARTESIAN_POINT('',(0.288675134594813,-0.96,0.));
#10152=CARTESIAN_POINT('',(0.288675134594813,-0.96,0.));
#10153=CARTESIAN_POINT('',(0.288675134594813,-0.6,0.));
#10154=CARTESIAN_POINT('Origin',(-0.144337567297406,-0.6,-0.25));
#10155=CARTESIAN_POINT('',(-0.144337567297406,-0.6,-0.25));
#10156=CARTESIAN_POINT('',(0.144337567297406,-0.6,-0.25));
#10157=CARTESIAN_POINT('',(-0.144337567297406,-0.96,-0.25));
#10158=CARTESIAN_POINT('',(-0.144337567297406,-0.6,-0.25));
#10159=CARTESIAN_POINT('',(0.144337567297406,-0.96,-0.25));
#10160=CARTESIAN_POINT('Origin',(-0.288675134594813,-0.6,-8.32667268468867E-17));
#10161=CARTESIAN_POINT('',(-0.288675134594813,-0.6,-3.53525079574969E-17));
#10162=CARTESIAN_POINT('',(-0.144337567297406,-0.6,-0.25));
#10163=CARTESIAN_POINT('',(-0.288675134594813,-0.96,-5.55111512312578E-17));
#10164=CARTESIAN_POINT('',(-0.288675134594813,-0.6,-3.53525079574969E-17));
#10165=CARTESIAN_POINT('',(-0.144337567297406,-0.96,-0.25));
#10166=CARTESIAN_POINT('Origin',(-0.144337567297407,-0.6,0.25));
#10167=CARTESIAN_POINT('',(-0.144337567297407,-0.6,0.25));
#10168=CARTESIAN_POINT('',(-0.288675134594813,-0.6,-3.53525079574969E-17));
#10169=CARTESIAN_POINT('',(-0.144337567297407,-0.96,0.25));
#10170=CARTESIAN_POINT('',(-0.144337567297407,-0.6,0.25));
#10171=CARTESIAN_POINT('',(-0.288675134594813,-0.96,-3.53525079574969E-17));
#10172=CARTESIAN_POINT('Origin',(0.144337567297406,-0.6,0.25));
#10173=CARTESIAN_POINT('',(0.144337567297406,-0.6,0.25));
#10174=CARTESIAN_POINT('',(-0.144337567297407,-0.6,0.25));
#10175=CARTESIAN_POINT('',(0.144337567297406,-0.96,0.25));
#10176=CARTESIAN_POINT('',(0.144337567297406,-0.6,0.25));
#10177=CARTESIAN_POINT('',(-0.144337567297407,-0.96,0.25));
#10178=CARTESIAN_POINT('Origin',(0.288675134594813,-0.6,0.));
#10179=CARTESIAN_POINT('',(0.144337567297406,-0.6,0.25));
#10180=CARTESIAN_POINT('',(0.144337567297406,-0.96,0.25));
#10181=CARTESIAN_POINT('Origin',(0.,-0.6,0.));
#10182=CARTESIAN_POINT('Origin',(0.,-0.96,0.));
#10183=CARTESIAN_POINT('Origin',(0.,-1.8,0.));
#10184=CARTESIAN_POINT('',(-0.2942,-1.8,3.60291088309151E-17));
#10185=CARTESIAN_POINT('Origin',(0.,-1.8,0.));
#10186=CARTESIAN_POINT('Origin',(0.45,0.6,0.));
#10187=CARTESIAN_POINT('',(-0.45,0.6,-5.51091059616309E-17));
#10188=CARTESIAN_POINT('Origin',(0.,0.6,0.));
#10189=CARTESIAN_POINT('Origin',(0.,0.575,0.));
#10190=CARTESIAN_POINT('',(-0.5,0.55,-6.12323399573677E-17));
#10191=CARTESIAN_POINT('Origin',(0.,0.55,0.));
#10192=CARTESIAN_POINT('',(-0.475,0.575,-5.81707229594993E-17));
#10193=CARTESIAN_POINT('Origin',(0.,0.29,0.));
#10194=CARTESIAN_POINT('',(-0.5,0.0299999999999998,-6.12323399573677E-17));
#10195=CARTESIAN_POINT('Origin',(0.,0.0299999999999998,0.));
#10196=CARTESIAN_POINT('',(-0.5,0.29,-6.12323399573677E-17));
#10197=CARTESIAN_POINT('Origin',(0.,0.0150000000000001,0.));
#10198=CARTESIAN_POINT('',(-0.47,7.11236625150491E-17,-5.75583995599256E-17));
#10199=CARTESIAN_POINT('Origin',(0.,0.,0.));
#10200=CARTESIAN_POINT('',(-0.485,0.0150000000000001,-5.93953697586466E-17));
#10201=CARTESIAN_POINT('Origin',(0.32,0.,0.));
#10202=CARTESIAN_POINT('',(-0.32,-6.93889390390723E-18,-3.91886975727153E-17));
#10203=CARTESIAN_POINT('Origin',(0.,0.,0.));
#10204=CARTESIAN_POINT('Origin',(0.,-0.02,0.));
#10205=CARTESIAN_POINT('',(-0.2942,-0.0515999999999999,3.60291088309151E-17));
#10206=CARTESIAN_POINT('Origin',(0.,-0.0515999999999999,0.));
#10207=CARTESIAN_POINT('',(-0.31,-0.02,-3.7964050773568E-17));
#10208=CARTESIAN_POINT('Origin',(0.,-1.24,0.));
#10209=CARTESIAN_POINT('',(-0.2942,-1.24,-3.60291088309151E-17));
#11506=UNCERTAINTY_MEASURE_WITH_UNIT(LENGTH_MEASURE(0.001),#11560,
'DISTANCE_ACCURACY_VALUE',
'Maximum model space distance between geometric entities at asserted c
onnectivities');
#11522=UNCERTAINTY_MEASURE_WITH_UNIT(LENGTH_MEASURE(0.001),#11560,
'DISTANCE_ACCURACY_VALUE',
'Maximum model space distance between geometric entities at asserted c
onnectivities');
#11543=(
GEOMETRIC_REPRESENTATION_CONTEXT(3)
GLOBAL_UNCERTAINTY_ASSIGNED_CONTEXT((#11506))
GLOBAL_UNIT_ASSIGNED_CONTEXT((#11560,#11562,#11563))
REPRESENTATION_CONTEXT('','3D')
);
#11559=(
GEOMETRIC_REPRESENTATION_CONTEXT(3)
GLOBAL_UNCERTAINTY_ASSIGNED_CONTEXT((#11522))
GLOBAL_UNIT_ASSIGNED_CONTEXT((#11560,#11562,#11563))
REPRESENTATION_CONTEXT('','3D')
);
#11560=(
LENGTH_UNIT()
NAMED_UNIT(*)
SI_UNIT(.CENTI.,.METRE.)
);
#11562=(
NAMED_UNIT(*)
PLANE_ANGLE_UNIT()
SI_UNIT($,.RADIAN.)
);
#11563=(
NAMED_UNIT(*)
SI_UNIT($,.STERADIAN.)
SOLID_ANGLE_UNIT()
);
#11584=SHAPE_DEFINITION_REPRESENTATION(#11620,#11741);
#11620=PRODUCT_DEFINITION_SHAPE('',$,#11778);
#11741=SHAPE_REPRESENTATION('',(#7013),#11543);
#11757=PRODUCT_DEFINITION_CONTEXT('part definition',#11867,'design');
#11778=PRODUCT_DEFINITION('M6x18 mounting screw','M6x18 mounting screw',
#11814,#11757);
#11814=PRODUCT_DEFINITION_FORMATION('',$,#11889);
#11867=APPLICATION_CONTEXT(
'Core Data for Automotive Mechanical Design Process');
#11868=PRODUCT_CONTEXT('part definition',#11867,'mechanical');
#11889=PRODUCT('M6x18 mounting screw','M6x18 mounting screw',
'M6x18 mounting screw',(#11868));
#11968=COLOUR_RGB('Black',0.12,0.14,0.17);
#11969=FILL_AREA_STYLE_COLOUR('',#11968);
#11970=FILL_AREA_STYLE('',(#11969));
#11971=SURFACE_STYLE_FILL_AREA(#11970);
#11972=SURFACE_SIDE_STYLE('',(#11971));
#11973=SURFACE_STYLE_USAGE(.BOTH.,#11972);
#11974=PRESENTATION_STYLE_ASSIGNMENT((#11973));
ENDSEC;
END-ISO-10303-21;
